ISO-10303-21;
HEADER;
FILE_DESCRIPTION((''),'2;1');
FILE_NAME('Clamp_Bolt_1.step','2026-10-09T10:15:02-07:00',(''),(''),'','','');
FILE_SCHEMA (('AUTOMOTIVE_DESIGN { 1 0 10303 214 3 1 1 }'));
ENDSEC;
DATA;
#10=MECHANICAL_DESIGN_GEOMETRIC_PRESENTATION_REPRESENTATION('',(#89),#6779);
#51=TOROIDAL_SURFACE('',#4342,4.4,0.6) ;
#52=TOROIDAL_SURFACE('',#4346,3.25,0.25) ;
#69=SHAPE_REPRESENTATION_RELATIONSHIP('SRR','None',#6823,#79) ;
#79=ADVANCED_BREP_SHAPE_REPRESENTATION('',(#99),#6775) ;
#89=STYLED_ITEM('',(#6877),#99) ;
#99=MANIFOLD_SOLID_BREP('Body1',#3901) ;
#127=FACE_BOUND('',#787,.T.) ;
#128=FACE_BOUND('',#789,.T.) ;
#223=PLANE('',#4328) ;
#224=PLANE('',#4329) ;
#225=PLANE('',#4330) ;
#226=PLANE('',#4331) ;
#227=PLANE('',#4332) ;
#228=PLANE('',#4333) ;
#229=PLANE('',#4334) ;
#230=PLANE('',#4335) ;
#231=PLANE('',#4337) ;
#232=PLANE('',#4340) ;
#323=CONICAL_SURFACE('',#4351,2.5,0.785398163397) ;
#511=FACE_OUTER_BOUND('',#779,.T.) ;
#512=FACE_OUTER_BOUND('',#780,.T.) ;
#513=FACE_OUTER_BOUND('',#781,.T.) ;
#514=FACE_OUTER_BOUND('',#782,.T.) ;
#515=FACE_OUTER_BOUND('',#783,.T.) ;
#516=FACE_OUTER_BOUND('',#784,.T.) ;
#517=FACE_OUTER_BOUND('',#785,.T.) ;
#518=FACE_OUTER_BOUND('',#786,.T.) ;
#519=FACE_OUTER_BOUND('',#788,.T.) ;
#520=FACE_OUTER_BOUND('',#790,.T.) ;
#521=FACE_OUTER_BOUND('',#791,.T.) ;
#522=FACE_OUTER_BOUND('',#792,.T.) ;
#523=FACE_OUTER_BOUND('',#793,.T.) ;
#524=FACE_OUTER_BOUND('',#794,.T.) ;
#525=FACE_OUTER_BOUND('',#795,.T.) ;
#779=EDGE_LOOP('',(#3363,#3364,#3365,#3366)) ;
#780=EDGE_LOOP('',(#3367,#3368,#3369,#3370)) ;
#781=EDGE_LOOP('',(#3371,#3372,#3373,#3374)) ;
#782=EDGE_LOOP('',(#3375,#3376,#3377,#3378,#3379,#3380)) ;
#783=EDGE_LOOP('',(#3381,#3382,#3383,#3384)) ;
#784=EDGE_LOOP('',(#3385,#3386,#3387,#3388)) ;
#785=EDGE_LOOP('',(#3389,#3390,#3391,#3392)) ;
#786=EDGE_LOOP('',(#3393)) ;
#787=EDGE_LOOP('',(#3394,#3395,#3396,#3397,#3398,#3399)) ;
#788=EDGE_LOOP('',(#3400)) ;
#789=EDGE_LOOP('',(#3401)) ;
#790=EDGE_LOOP('',(#3402)) ;
#791=EDGE_LOOP('',(#3403,#3404,#3405,#3406)) ;
#792=EDGE_LOOP('',(#3407,#3408,#3409,#3410)) ;
#793=EDGE_LOOP('',(#3411,#3412,#3413,#3414)) ;
#794=EDGE_LOOP('',(#3415,#3416,#3417,#3418)) ;
#795=EDGE_LOOP('',(#3419,#3420,#3421,#3422)) ;
#1123=LINE('',#6490,#1483) ;
#1124=LINE('',#6492,#1484) ;
#1125=LINE('',#6494,#1485) ;
#1126=LINE('',#6495,#1486) ;
#1127=LINE('',#6499,#1487) ;
#1128=LINE('',#6500,#1488) ;
#1129=LINE('',#6501,#1489) ;
#1130=LINE('',#6504,#1490) ;
#1131=LINE('',#6506,#1491) ;
#1132=LINE('',#6507,#1492) ;
#1133=LINE('',#6510,#1493) ;
#1134=LINE('',#6512,#1494) ;
#1135=LINE('',#6513,#1495) ;
#1136=LINE('',#6516,#1496) ;
#1137=LINE('',#6517,#1497) ;
#1138=LINE('',#6520,#1498) ;
#1139=LINE('',#6521,#1499) ;
#1140=LINE('',#6523,#1500) ;
#1141=LINE('',#6540,#1501) ;
#1142=LINE('',#6547,#1502) ;
#1143=LINE('',#6550,#1503) ;
#1483=VECTOR('',#5339,1.) ;
#1484=VECTOR('',#5340,1.) ;
#1485=VECTOR('',#5341,1.) ;
#1486=VECTOR('',#5342,1.) ;
#1487=VECTOR('',#5345,1.) ;
#1488=VECTOR('',#5346,0.99999999999962) ;
#1489=VECTOR('',#5347,0.99999999999962) ;
#1490=VECTOR('',#5350,0.99999999999962) ;
#1491=VECTOR('',#5351,1.) ;
#1492=VECTOR('',#5352,0.99999999999962) ;
#1493=VECTOR('',#5355,0.99999999999962) ;
#1494=VECTOR('',#5356,1.) ;
#1495=VECTOR('',#5357,0.99999999999962) ;
#1496=VECTOR('',#5360,1.) ;
#1497=VECTOR('',#5361,0.99999999999962) ;
#1498=VECTOR('',#5364,0.99999999999962) ;
#1499=VECTOR('',#5365,1.) ;
#1500=VECTOR('',#5368,1.) ;
#1501=VECTOR('',#5391,5.) ;
#1502=VECTOR('',#5400,3.) ;
#1503=VECTOR('',#5405,2.5) ;
#1687=CIRCLE('',#4336,4.4) ;
#1688=CIRCLE('',#4338,5.) ;
#1689=CIRCLE('',#4339,3.25) ;
#1690=CIRCLE('',#4341,2.5) ;
#1691=CIRCLE('',#4343,0.6) ;
#1692=CIRCLE('',#4344,5.) ;
#1693=CIRCLE('',#4347,0.25) ;
#1694=CIRCLE('',#4348,3.) ;
#1695=CIRCLE('',#4350,3.) ;
#1955=VERTEX_POINT('',#6488) ;
#1956=VERTEX_POINT('',#6489) ;
#1957=VERTEX_POINT('',#6491) ;
#1958=VERTEX_POINT('',#6493) ;
#1959=VERTEX_POINT('',#6497) ;
#1960=VERTEX_POINT('',#6498) ;
#1961=VERTEX_POINT('',#6503) ;
#1962=VERTEX_POINT('',#6505) ;
#1963=VERTEX_POINT('',#6509) ;
#1964=VERTEX_POINT('',#6511) ;
#1965=VERTEX_POINT('',#6515) ;
#1966=VERTEX_POINT('',#6519) ;
#1967=VERTEX_POINT('',#6525) ;
#1968=VERTEX_POINT('',#6528) ;
#1969=VERTEX_POINT('',#6530) ;
#1970=VERTEX_POINT('',#6533) ;
#1971=VERTEX_POINT('',#6536) ;
#1972=VERTEX_POINT('',#6542) ;
#1973=VERTEX_POINT('',#6546) ;
#2435=EDGE_CURVE('',#1955,#1956,#1123,.T.) ;
#2436=EDGE_CURVE('',#1955,#1957,#1124,.T.) ;
#2437=EDGE_CURVE('',#1957,#1958,#1125,.T.) ;
#2438=EDGE_CURVE('',#1956,#1958,#1126,.T.) ;
#2439=EDGE_CURVE('',#1959,#1960,#1127,.T.) ;
#2440=EDGE_CURVE('',#1959,#1955,#1128,.T.) ;
#2441=EDGE_CURVE('',#1960,#1956,#1129,.T.) ;
#2442=EDGE_CURVE('',#1957,#1961,#1130,.T.) ;
#2443=EDGE_CURVE('',#1961,#1962,#1131,.T.) ;
#2444=EDGE_CURVE('',#1958,#1962,#1132,.T.) ;
#2445=EDGE_CURVE('',#1962,#1963,#1133,.T.) ;
#2446=EDGE_CURVE('',#1963,#1964,#1134,.T.) ;
#2447=EDGE_CURVE('',#1964,#1960,#1135,.T.) ;
#2448=EDGE_CURVE('',#1965,#1964,#1136,.T.) ;
#2449=EDGE_CURVE('',#1965,#1959,#1137,.T.) ;
#2450=EDGE_CURVE('',#1961,#1966,#1138,.T.) ;
#2451=EDGE_CURVE('',#1966,#1963,#1139,.T.) ;
#2452=EDGE_CURVE('',#1966,#1965,#1140,.T.) ;
#2453=EDGE_CURVE('',#1967,#1967,#1687,.T.) ;
#2454=EDGE_CURVE('',#1968,#1968,#1688,.T.) ;
#2455=EDGE_CURVE('',#1969,#1969,#1689,.T.) ;
#2456=EDGE_CURVE('',#1970,#1970,#1690,.T.) ;
#2457=EDGE_CURVE('',#1967,#1971,#1691,.T.) ;
#2458=EDGE_CURVE('',#1971,#1971,#1692,.T.) ;
#2459=EDGE_CURVE('',#1971,#1968,#1141,.T.) ;
#2460=EDGE_CURVE('',#1969,#1972,#1693,.T.) ;
#2461=EDGE_CURVE('',#1972,#1972,#1694,.T.) ;
#2462=EDGE_CURVE('',#1972,#1973,#1142,.T.) ;
#2463=EDGE_CURVE('',#1973,#1973,#1695,.T.) ;
#2464=EDGE_CURVE('',#1973,#1970,#1143,.T.) ;
#3363=ORIENTED_EDGE('',*,*,#2435,.F.) ;
#3364=ORIENTED_EDGE('',*,*,#2436,.T.) ;
#3365=ORIENTED_EDGE('',*,*,#2437,.T.) ;
#3366=ORIENTED_EDGE('',*,*,#2438,.F.) ;
#3367=ORIENTED_EDGE('',*,*,#2439,.F.) ;
#3368=ORIENTED_EDGE('',*,*,#2440,.T.) ;
#3369=ORIENTED_EDGE('',*,*,#2435,.T.) ;
#3370=ORIENTED_EDGE('',*,*,#2441,.F.) ;
#3371=ORIENTED_EDGE('',*,*,#2437,.F.) ;
#3372=ORIENTED_EDGE('',*,*,#2442,.T.) ;
#3373=ORIENTED_EDGE('',*,*,#2443,.T.) ;
#3374=ORIENTED_EDGE('',*,*,#2444,.F.) ;
#3375=ORIENTED_EDGE('',*,*,#2438,.T.) ;
#3376=ORIENTED_EDGE('',*,*,#2444,.T.) ;
#3377=ORIENTED_EDGE('',*,*,#2445,.T.) ;
#3378=ORIENTED_EDGE('',*,*,#2446,.T.) ;
#3379=ORIENTED_EDGE('',*,*,#2447,.T.) ;
#3380=ORIENTED_EDGE('',*,*,#2441,.T.) ;
#3381=ORIENTED_EDGE('',*,*,#2448,.F.) ;
#3382=ORIENTED_EDGE('',*,*,#2449,.T.) ;
#3383=ORIENTED_EDGE('',*,*,#2439,.T.) ;
#3384=ORIENTED_EDGE('',*,*,#2447,.F.) ;
#3385=ORIENTED_EDGE('',*,*,#2443,.F.) ;
#3386=ORIENTED_EDGE('',*,*,#2450,.T.) ;
#3387=ORIENTED_EDGE('',*,*,#2451,.T.) ;
#3388=ORIENTED_EDGE('',*,*,#2445,.F.) ;
#3389=ORIENTED_EDGE('',*,*,#2451,.F.) ;
#3390=ORIENTED_EDGE('',*,*,#2452,.T.) ;
#3391=ORIENTED_EDGE('',*,*,#2448,.T.) ;
#3392=ORIENTED_EDGE('',*,*,#2446,.F.) ;
#3393=ORIENTED_EDGE('',*,*,#2453,.T.) ;
#3394=ORIENTED_EDGE('',*,*,#2449,.F.) ;
#3395=ORIENTED_EDGE('',*,*,#2452,.F.) ;
#3396=ORIENTED_EDGE('',*,*,#2450,.F.) ;
#3397=ORIENTED_EDGE('',*,*,#2442,.F.) ;
#3398=ORIENTED_EDGE('',*,*,#2436,.F.) ;
#3399=ORIENTED_EDGE('',*,*,#2440,.F.) ;
#3400=ORIENTED_EDGE('',*,*,#2454,.F.) ;
#3401=ORIENTED_EDGE('',*,*,#2455,.T.) ;
#3402=ORIENTED_EDGE('',*,*,#2456,.F.) ;
#3403=ORIENTED_EDGE('',*,*,#2453,.F.) ;
#3404=ORIENTED_EDGE('',*,*,#2457,.T.) ;
#3405=ORIENTED_EDGE('',*,*,#2458,.T.) ;
#3406=ORIENTED_EDGE('',*,*,#2457,.F.) ;
#3407=ORIENTED_EDGE('',*,*,#2458,.F.) ;
#3408=ORIENTED_EDGE('',*,*,#2459,.T.) ;
#3409=ORIENTED_EDGE('',*,*,#2454,.T.) ;
#3410=ORIENTED_EDGE('',*,*,#2459,.F.) ;
#3411=ORIENTED_EDGE('',*,*,#2455,.F.) ;
#3412=ORIENTED_EDGE('',*,*,#2460,.T.) ;
#3413=ORIENTED_EDGE('',*,*,#2461,.T.) ;
#3414=ORIENTED_EDGE('',*,*,#2460,.F.) ;
#3415=ORIENTED_EDGE('',*,*,#2461,.F.) ;
#3416=ORIENTED_EDGE('',*,*,#2462,.T.) ;
#3417=ORIENTED_EDGE('',*,*,#2463,.T.) ;
#3418=ORIENTED_EDGE('',*,*,#2462,.F.) ;
#3419=ORIENTED_EDGE('',*,*,#2463,.F.) ;
#3420=ORIENTED_EDGE('',*,*,#2464,.T.) ;
#3421=ORIENTED_EDGE('',*,*,#2456,.T.) ;
#3422=ORIENTED_EDGE('',*,*,#2464,.F.) ;
#3643=CYLINDRICAL_SURFACE('',#4345,5.) ;
#3644=CYLINDRICAL_SURFACE('',#4349,3.) ;
#3835=ADVANCED_FACE('',(#511),#223,.T.) ;
#3836=ADVANCED_FACE('',(#512),#224,.T.) ;
#3837=ADVANCED_FACE('',(#513),#225,.T.) ;
#3838=ADVANCED_FACE('',(#514),#226,.T.) ;
#3839=ADVANCED_FACE('',(#515),#227,.T.) ;
#3840=ADVANCED_FACE('',(#516),#228,.T.) ;
#3841=ADVANCED_FACE('',(#517),#229,.T.) ;
#3842=ADVANCED_FACE('',(#518,#127),#230,.T.) ;
#3843=ADVANCED_FACE('',(#519,#128),#231,.F.) ;
#3844=ADVANCED_FACE('',(#520),#232,.F.) ;
#3845=ADVANCED_FACE('',(#521),#51,.T.) ;
#3846=ADVANCED_FACE('',(#522),#3643,.T.) ;
#3847=ADVANCED_FACE('',(#523),#52,.F.) ;
#3848=ADVANCED_FACE('',(#524),#3644,.T.) ;
#3849=ADVANCED_FACE('',(#525),#323,.T.) ;
#3901=CLOSED_SHELL('',(#3835,#3836,#3837,#3838,#3839,#3840,#3841,#3842,
#3843,#3844,#3845,#3846,#3847,#3848,#3849)) ;
#4327=AXIS2_PLACEMENT_3D('',#6486,#5335,#5336) ;
#4328=AXIS2_PLACEMENT_3D('',#6487,#5337,#5338) ;
#4329=AXIS2_PLACEMENT_3D('',#6496,#5343,#5344) ;
#4330=AXIS2_PLACEMENT_3D('',#6502,#5348,#5349) ;
#4331=AXIS2_PLACEMENT_3D('',#6508,#5353,#5354) ;
#4332=AXIS2_PLACEMENT_3D('',#6514,#5358,#5359) ;
#4333=AXIS2_PLACEMENT_3D('',#6518,#5362,#5363) ;
#4334=AXIS2_PLACEMENT_3D('',#6522,#5366,#5367) ;
#4335=AXIS2_PLACEMENT_3D('',#6524,#5369,#5370) ;
#4336=AXIS2_PLACEMENT_3D('',#6526,#5371,#5372) ;
#4337=AXIS2_PLACEMENT_3D('',#6527,#5373,#5374) ;
#4338=AXIS2_PLACEMENT_3D('',#6529,#5375,#5376) ;
#4339=AXIS2_PLACEMENT_3D('',#6531,#5377,#5378) ;
#4340=AXIS2_PLACEMENT_3D('',#6532,#5379,#5380) ;
#4341=AXIS2_PLACEMENT_3D('',#6534,#5381,#5382) ;
#4342=AXIS2_PLACEMENT_3D('',#6535,#5383,#5384) ;
#4343=AXIS2_PLACEMENT_3D('',#6537,#5385,#5386) ;
#4344=AXIS2_PLACEMENT_3D('',#6538,#5387,#5388) ;
#4345=AXIS2_PLACEMENT_3D('',#6539,#5389,#5390) ;
#4346=AXIS2_PLACEMENT_3D('',#6541,#5392,#5393) ;
#4347=AXIS2_PLACEMENT_3D('',#6543,#5394,#5395) ;
#4348=AXIS2_PLACEMENT_3D('',#6544,#5396,#5397) ;
#4349=AXIS2_PLACEMENT_3D('',#6545,#5398,#5399) ;
#4350=AXIS2_PLACEMENT_3D('',#6548,#5401,#5402) ;
#4351=AXIS2_PLACEMENT_3D('',#6549,#5403,#5404) ;
#5335=DIRECTION('axis',(0.,0.,1.)) ;
#5336=DIRECTION('refdir',(1.,0.,0.)) ;
#5337=DIRECTION('center_axis',(1.,0.,-1.53837014911E-16)) ;
#5338=DIRECTION('ref_axis',(-1.53837014911E-16,0.,-1.)) ;
#5339=DIRECTION('',(0.,1.,0.)) ;
#5340=DIRECTION('',(0.,0.,-1.)) ;
#5341=DIRECTION('',(0.,1.,0.)) ;
#5342=DIRECTION('',(0.,0.,-1.)) ;
#5343=DIRECTION('center_axis',(0.50000000000019,0.,-0.866025403784329)) ;
#5344=DIRECTION('ref_axis',(-0.866025403784329,0.,-0.50000000000019)) ;
#5345=DIRECTION('',(0.,1.,0.)) ;
#5346=DIRECTION('',(-0.866025403784329,0.,-0.50000000000019)) ;
#5347=DIRECTION('',(-0.866025403784329,0.,-0.50000000000019)) ;
#5348=DIRECTION('center_axis',(0.50000000000019,0.,0.866025403784329)) ;
#5349=DIRECTION('ref_axis',(0.866025403784329,0.,-0.50000000000019)) ;
#5350=DIRECTION('',(0.866025403784329,0.,-0.50000000000019)) ;
#5351=DIRECTION('',(0.,1.,0.)) ;
#5352=DIRECTION('',(0.866025403784329,0.,-0.50000000000019)) ;
#5353=DIRECTION('center_axis',(0.,-1.,0.)) ;
#5354=DIRECTION('ref_axis',(1.,0.,0.)) ;
#5355=DIRECTION('',(0.866025403784329,0.,0.50000000000019)) ;
#5356=DIRECTION('',(0.,0.,1.)) ;
#5357=DIRECTION('',(-0.866025403784329,0.,0.50000000000019)) ;
#5358=DIRECTION('center_axis',(-0.50000000000019,0.,-0.866025403784329)) ;
#5359=DIRECTION('ref_axis',(-0.866025403784329,0.,0.50000000000019)) ;
#5360=DIRECTION('',(0.,1.,0.)) ;
#5361=DIRECTION('',(-0.866025403784329,0.,0.50000000000019)) ;
#5362=DIRECTION('center_axis',(-0.50000000000019,0.,0.866025403784329)) ;
#5363=DIRECTION('ref_axis',(0.866025403784329,0.,0.50000000000019)) ;
#5364=DIRECTION('',(0.866025403784329,0.,0.50000000000019)) ;
#5365=DIRECTION('',(0.,1.,0.)) ;
#5366=DIRECTION('center_axis',(-1.,0.,0.)) ;
#5367=DIRECTION('ref_axis',(0.,0.,1.)) ;
#5368=DIRECTION('',(0.,0.,1.)) ;
#5369=DIRECTION('center_axis',(0.,-1.,0.)) ;
#5370=DIRECTION('ref_axis',(-1.,0.,0.)) ;
#5371=DIRECTION('center_axis',(0.,-1.,0.)) ;
#5372=DIRECTION('ref_axis',(0.,0.,1.)) ;
#5373=DIRECTION('center_axis',(0.,-1.,0.)) ;
#5374=DIRECTION('ref_axis',(-1.,0.,0.)) ;
#5375=DIRECTION('center_axis',(0.,-1.,0.)) ;
#5376=DIRECTION('ref_axis',(0.,0.,1.)) ;
#5377=DIRECTION('center_axis',(0.,-1.,0.)) ;
#5378=DIRECTION('ref_axis',(0.,0.,1.)) ;
#5379=DIRECTION('center_axis',(0.,-1.,0.)) ;
#5380=DIRECTION('ref_axis',(-1.,0.,0.)) ;
#5381=DIRECTION('center_axis',(0.,-1.,0.)) ;
#5382=DIRECTION('ref_axis',(0.,0.,1.)) ;
#5383=DIRECTION('center_axis',(0.,-1.,0.)) ;
#5384=DIRECTION('ref_axis',(0.479425538604205,0.,-0.877582561890372)) ;
#5385=DIRECTION('center_axis',(-0.877582561890372,0.,-0.479425538604205)) ;
#5386=DIRECTION('ref_axis',(-0.479425538604205,0.,0.877582561890372)) ;
#5387=DIRECTION('center_axis',(0.,-1.,0.)) ;
#5388=DIRECTION('ref_axis',(0.,0.,1.)) ;
#5389=DIRECTION('center_axis',(0.,-1.,0.)) ;
#5390=DIRECTION('ref_axis',(0.479425538604204,0.,-0.877582561890372)) ;
#5391=DIRECTION('',(0.,1.,0.)) ;
#5392=DIRECTION('center_axis',(0.,-1.,0.)) ;
#5393=DIRECTION('ref_axis',(0.479425538604204,0.,-0.877582561890372)) ;
#5394=DIRECTION('center_axis',(0.877582561890372,0.,0.479425538604204)) ;
#5395=DIRECTION('ref_axis',(-0.479425538604204,0.,0.877582561890372)) ;
#5396=DIRECTION('center_axis',(0.,-1.,0.)) ;
#5397=DIRECTION('ref_axis',(0.,0.,1.)) ;
#5398=DIRECTION('center_axis',(0.,-1.,0.)) ;
#5399=DIRECTION('ref_axis',(0.479425538604204,0.,-0.877582561890372)) ;
#5400=DIRECTION('',(0.,1.,0.)) ;
#5401=DIRECTION('center_axis',(0.,-1.,0.)) ;
#5402=DIRECTION('ref_axis',(0.,0.,1.)) ;
#5403=DIRECTION('center_axis',(0.,-1.,0.)) ;
#5404=DIRECTION('ref_axis',(0.479425538604204,0.,-0.877582561890372)) ;
#5405=DIRECTION('',(0.339005049420894,0.707106781186865,-0.620544580563467)) ;
#6486=CARTESIAN_POINT('',(0.,0.,0.)) ;
#6487=CARTESIAN_POINT('Origin',(-37.5,-26.,11.443375673)) ;
#6488=CARTESIAN_POINT('',(-37.5,-26.,11.443375673)) ;
#6489=CARTESIAN_POINT('',(-37.5,-23.,11.443375673)) ;
#6490=CARTESIAN_POINT('',(-37.5,-24.5,11.443375673)) ;
#6491=CARTESIAN_POINT('',(-37.5,-26.,8.55662432703)) ;
#6492=CARTESIAN_POINT('',(-37.5,-26.,10.)) ;
#6493=CARTESIAN_POINT('',(-37.5,-23.,8.55662432703)) ;
#6494=CARTESIAN_POINT('',(-37.5,-24.5,8.55662432703)) ;
#6495=CARTESIAN_POINT('',(-37.5,-23.,10.)) ;
#6496=CARTESIAN_POINT('Origin',(-35.,-26.,12.8867513459)) ;
#6497=CARTESIAN_POINT('',(-35.,-26.,12.8867513459)) ;
#6498=CARTESIAN_POINT('',(-35.,-23.,12.8867513459)) ;
#6499=CARTESIAN_POINT('',(-35.,-24.5,12.8867513459)) ;
#6500=CARTESIAN_POINT('',(-36.25,-26.,12.1650635095)) ;
#6501=CARTESIAN_POINT('',(-36.25,-23.,12.1650635095)) ;
#6502=CARTESIAN_POINT('Origin',(-37.5,-26.,8.55662432703)) ;
#6503=CARTESIAN_POINT('',(-35.,-26.,7.11324865405)) ;
#6504=CARTESIAN_POINT('',(-36.25,-26.,7.83493649054)) ;
#6505=CARTESIAN_POINT('',(-35.,-23.,7.11324865405)) ;
#6506=CARTESIAN_POINT('',(-35.,-24.5,7.11324865405)) ;
#6507=CARTESIAN_POINT('',(-36.25,-23.,7.83493649054)) ;
#6508=CARTESIAN_POINT('Origin',(-35.,-23.,10.)) ;
#6509=CARTESIAN_POINT('',(-32.5,-23.,8.55662432703)) ;
#6510=CARTESIAN_POINT('',(-33.75,-23.,7.83493649054)) ;
#6511=CARTESIAN_POINT('',(-32.5,-23.,11.443375673)) ;
#6512=CARTESIAN_POINT('',(-32.5,-23.,10.)) ;
#6513=CARTESIAN_POINT('',(-33.75,-23.,12.1650635095)) ;
#6514=CARTESIAN_POINT('Origin',(-32.5,-26.,11.443375673)) ;
#6515=CARTESIAN_POINT('',(-32.5,-26.,11.443375673)) ;
#6516=CARTESIAN_POINT('',(-32.5,-24.5,11.443375673)) ;
#6517=CARTESIAN_POINT('',(-33.75,-26.,12.1650635095)) ;
#6518=CARTESIAN_POINT('Origin',(-35.,-26.,7.11324865405)) ;
#6519=CARTESIAN_POINT('',(-32.5,-26.,8.55662432703)) ;
#6520=CARTESIAN_POINT('',(-33.75,-26.,7.83493649054)) ;
#6521=CARTESIAN_POINT('',(-32.5,-24.5,8.55662432703)) ;
#6522=CARTESIAN_POINT('Origin',(-32.5,-26.,8.55662432703)) ;
#6523=CARTESIAN_POINT('',(-32.5,-26.,10.)) ;
#6524=CARTESIAN_POINT('Origin',(-35.,-26.,10.)) ;
#6525=CARTESIAN_POINT('',(-37.1094723699,-26.,13.8613632723)) ;
#6526=CARTESIAN_POINT('Origin',(-35.,-26.,10.)) ;
#6527=CARTESIAN_POINT('Origin',(-35.,-20.,5.)) ;
#6528=CARTESIAN_POINT('',(-37.397127693,-20.,14.3879128095)) ;
#6529=CARTESIAN_POINT('Origin',(-35.,-20.,10.)) ;
#6530=CARTESIAN_POINT('',(-36.5581330005,-20.,12.8521433261)) ;
#6531=CARTESIAN_POINT('Origin',(-35.,-20.,10.)) ;
#6532=CARTESIAN_POINT('Origin',(-35.,40.,7.5)) ;
#6533=CARTESIAN_POINT('',(-36.1985638465,40.,12.1939564047)) ;
#6534=CARTESIAN_POINT('Origin',(-35.,40.,10.)) ;
#6535=CARTESIAN_POINT('Origin',(-35.,-25.4,10.)) ;
#6536=CARTESIAN_POINT('',(-37.397127693,-25.4,14.3879128095)) ;
#6537=CARTESIAN_POINT('Origin',(-37.1094723698585,-25.4,13.8613632723176)) ;
#6538=CARTESIAN_POINT('Origin',(-35.,-25.4,10.)) ;
#6539=CARTESIAN_POINT('Origin',(-35.,7.,10.)) ;
#6540=CARTESIAN_POINT('',(-37.397127693021,7.,14.3879128094519)) ;
#6541=CARTESIAN_POINT('Origin',(-35.,-19.75,10.)) ;
#6542=CARTESIAN_POINT('',(-36.4382766158,-19.75,12.6327476857)) ;
#6543=CARTESIAN_POINT('Origin',(-36.5581330004637,-19.75,12.8521433261437)) ;
#6544=CARTESIAN_POINT('Origin',(-35.,-19.75,10.)) ;
#6545=CARTESIAN_POINT('Origin',(-35.,7.,10.)) ;
#6546=CARTESIAN_POINT('',(-36.4382766158,39.5,12.6327476857)) ;
#6547=CARTESIAN_POINT('',(-36.4382766158126,7.,12.6327476856711)) ;
#6548=CARTESIAN_POINT('Origin',(-35.,39.5,10.)) ;
#6549=CARTESIAN_POINT('Origin',(-35.,40.,10.)) ;
#6550=CARTESIAN_POINT('',(-36.1985638465105,40.,12.1939564047259)) ;
#6763=UNCERTAINTY_MEASURE_WITH_UNIT(LENGTH_MEASURE(0.01),#6780,
'DISTANCE_ACCURACY_VALUE',
'Maximum model space distance between geometric entities at asserted c
onnectivities') ;
#6767=UNCERTAINTY_MEASURE_WITH_UNIT(LENGTH_MEASURE(0.01),#6780,
'DISTANCE_ACCURACY_VALUE',
'Maximum model space distance between geometric entities at asserted c
onnectivities') ;
#6775=(
GEOMETRIC_REPRESENTATION_CONTEXT(3)
GLOBAL_UNCERTAINTY_ASSIGNED_CONTEXT((#6763))
GLOBAL_UNIT_ASSIGNED_CONTEXT((#6780,#6782,#6783))
REPRESENTATION_CONTEXT('','3D')
) ;
#6779=(
GEOMETRIC_REPRESENTATION_CONTEXT(3)
GLOBAL_UNCERTAINTY_ASSIGNED_CONTEXT((#6767))
GLOBAL_UNIT_ASSIGNED_CONTEXT((#6780,#6782,#6783))
REPRESENTATION_CONTEXT('','3D')
) ;
#6780=(
LENGTH_UNIT()
NAMED_UNIT(*)
SI_UNIT(.MILLI.,.METRE.)
) ;
#6782=(
NAMED_UNIT(*)
PLANE_ANGLE_UNIT()
SI_UNIT($,.RADIAN.)
) ;
#6783=(
NAMED_UNIT(*)
SI_UNIT($,.STERADIAN.)
SOLID_ANGLE_UNIT()
) ;
#6791=SHAPE_DEFINITION_REPRESENTATION(#6802,#6823) ;
#6802=PRODUCT_DEFINITION_SHAPE('',$,#6835) ;
#6823=SHAPE_REPRESENTATION('',(#4327),#6775) ;
#6827=PRODUCT_DEFINITION_CONTEXT('part definition',#6862,'design') ;
#6835=PRODUCT_DEFINITION('Clamp_Bolt_1','Clamp_Bolt_1',#6846,#6827) ;
#6846=PRODUCT_DEFINITION_FORMATION('',$,#6871) ;
#6862=APPLICATION_CONTEXT(
'Core Data for Automotive Mechanical Design Process') ;
#6863=PRODUCT_CONTEXT('part definition',#6862,'mechanical') ;
#6871=PRODUCT('Clamp_Bolt_1','Clamp_Bolt_1',$,(#6863)) ;
#6877=PRESENTATION_STYLE_ASSIGNMENT((#6880)) ;
#6880=SURFACE_STYLE_USAGE(.BOTH.,#6883) ;
#6883=SURFACE_SIDE_STYLE('',(#6886)) ;
#6886=SURFACE_STYLE_FILL_AREA(#6889) ;
#6889=FILL_AREA_STYLE('Opaque(203,203,203)',(#6892)) ;
#6892=FILL_AREA_STYLE_COLOUR('Opaque(203,203,203)',#6895) ;
#6895=COLOUR_RGB('Opaque(203,203,203)', 0.31764706, 0.68627451, 0.89019608) ;
ENDSEC;
END-ISO-10303-21;
